ISO-10303-21;
HEADER;
/* Generated by software containing ST-Developer
 * from STEP Tools, Inc. (www.steptools.com) 
 */

FILE_DESCRIPTION(
/* description */ ('Bin tilter linkage'),
/* implementation_level */ '2;1');

FILE_NAME(
/* name */ 'M4 short cap screw (15).step',
/* time_stamp */ '2026-10-28T03:26:24-07:00',
/* author */ (''),
/* organization */ (''),
/* preprocessor_version */ 'ST-DEVELOPER v20.2',
/* originating_system */ 'Autodesk Translation Framework v15.17.0.0',
/* authorisation */ '');

FILE_SCHEMA (('AUTOMOTIVE_DESIGN { 1 0 10303 214 3 1 1 }'));
ENDSEC;

DATA;
#10=MECHANICAL_DESIGN_GEOMETRIC_PRESENTATION_REPRESENTATION('',(#912),#23728);
#700=SHAPE_REPRESENTATION_RELATIONSHIP('SRR','None',#24165,#806);
#806=ADVANCED_BREP_SHAPE_REPRESENTATION('',(#1025),#23665);
#912=STYLED_ITEM('',(#24772),#1025);
#1025=MANIFOLD_SOLID_BREP('Body1',#12443);
#1309=FACE_BOUND('',#3262,.T.);
#1674=PLANE('',#14478);
#1675=PLANE('',#14483);
#1676=PLANE('',#14486);
#2262=FACE_OUTER_BOUND('',#3261,.T.);
#2263=FACE_OUTER_BOUND('',#3263,.T.);
#2264=FACE_OUTER_BOUND('',#3264,.T.);
#2265=FACE_OUTER_BOUND('',#3265,.T.);
#2266=FACE_OUTER_BOUND('',#3266,.T.);
#3261=EDGE_LOOP('',(#9781));
#3262=EDGE_LOOP('',(#9782));
#3263=EDGE_LOOP('',(#9783,#9784,#9785,#9786));
#3264=EDGE_LOOP('',(#9787));
#3265=EDGE_LOOP('',(#9788,#9789,#9790,#9791));
#3266=EDGE_LOOP('',(#9792));
#4177=LINE('',#21351,#4852);
#4178=LINE('',#21355,#4853);
#4852=VECTOR('',#17416,0.35);
#4853=VECTOR('',#17421,0.199999999999999);
#5575=CIRCLE('',#14479,0.35);
#5576=CIRCLE('',#14480,0.199999999999999);
#5577=CIRCLE('',#14482,0.35);
#5578=CIRCLE('',#14485,0.199999999999999);
#6425=VERTEX_POINT('',#21344);
#6426=VERTEX_POINT('',#21346);
#6427=VERTEX_POINT('',#21349);
#6428=VERTEX_POINT('',#21354);
#7630=EDGE_CURVE('',#6425,#6425,#5575,.T.);
#7631=EDGE_CURVE('',#6426,#6426,#5576,.T.);
#7632=EDGE_CURVE('',#6427,#6427,#5577,.T.);
#7633=EDGE_CURVE('',#6427,#6425,#4177,.T.);
#7634=EDGE_CURVE('',#6426,#6428,#4178,.T.);
#7635=EDGE_CURVE('',#6428,#6428,#5578,.T.);
#9781=ORIENTED_EDGE('',*,*,#7630,.F.);
#9782=ORIENTED_EDGE('',*,*,#7631,.T.);
#9783=ORIENTED_EDGE('',*,*,#7632,.F.);
#9784=ORIENTED_EDGE('',*,*,#7633,.T.);
#9785=ORIENTED_EDGE('',*,*,#7630,.T.);
#9786=ORIENTED_EDGE('',*,*,#7633,.F.);
#9787=ORIENTED_EDGE('',*,*,#7632,.T.);
#9788=ORIENTED_EDGE('',*,*,#7631,.F.);
#9789=ORIENTED_EDGE('',*,*,#7634,.T.);
#9790=ORIENTED_EDGE('',*,*,#7635,.T.);
#9791=ORIENTED_EDGE('',*,*,#7634,.F.);
#9792=ORIENTED_EDGE('',*,*,#7635,.F.);
#11453=CYLINDRICAL_SURFACE('',#14481,0.35);
#11454=CYLINDRICAL_SURFACE('',#14484,0.199999999999999);
#11987=ADVANCED_FACE('',(#2262,#1309),#1674,.F.);
#11988=ADVANCED_FACE('',(#2263),#11453,.T.);
#11989=ADVANCED_FACE('',(#2264),#1675,.T.);
#11990=ADVANCED_FACE('',(#2265),#11454,.T.);
#11991=ADVANCED_FACE('',(#2266),#1676,.F.);
#12443=CLOSED_SHELL('',(#11987,#11988,#11989,#11990,#11991));
#14477=AXIS2_PLACEMENT_3D('',#21342,#17404,#17405);
#14478=AXIS2_PLACEMENT_3D('',#21343,#17406,#17407);
#14479=AXIS2_PLACEMENT_3D('',#21345,#17408,#17409);
#14480=AXIS2_PLACEMENT_3D('',#21347,#17410,#17411);
#14481=AXIS2_PLACEMENT_3D('',#21348,#17412,#17413);
#14482=AXIS2_PLACEMENT_3D('',#21350,#17414,#17415);
#14483=AXIS2_PLACEMENT_3D('',#21352,#17417,#17418);
#14484=AXIS2_PLACEMENT_3D('',#21353,#17419,#17420);
#14485=AXIS2_PLACEMENT_3D('',#21356,#17422,#17423);
#14486=AXIS2_PLACEMENT_3D('',#21357,#17424,#17425);
#17404=DIRECTION('axis',(0.,0.,1.));
#17405=DIRECTION('refdir',(1.,0.,0.));
#17406=DIRECTION('center_axis',(0.,1.,0.));
#17407=DIRECTION('ref_axis',(1.,0.,0.));
#17408=DIRECTION('center_axis',(0.,1.,0.));
#17409=DIRECTION('ref_axis',(1.,0.,0.));
#17410=DIRECTION('center_axis',(0.,1.,0.));
#17411=DIRECTION('ref_axis',(1.,0.,0.));
#17412=DIRECTION('center_axis',(0.,1.,0.));
#17413=DIRECTION('ref_axis',(1.,0.,0.));
#17414=DIRECTION('center_axis',(0.,1.,0.));
#17415=DIRECTION('ref_axis',(1.,0.,0.));
#17416=DIRECTION('',(0.,-1.,0.));
#17417=DIRECTION('center_axis',(0.,1.,0.));
#17418=DIRECTION('ref_axis',(1.,0.,0.));
#17419=DIRECTION('center_axis',(0.,1.,0.));
#17420=DIRECTION('ref_axis',(1.,0.,0.));
#17421=DIRECTION('',(0.,-1.,0.));
#17422=DIRECTION('center_axis',(0.,1.,0.));
#17423=DIRECTION('ref_axis',(1.,0.,0.));
#17424=DIRECTION('center_axis',(0.,1.,0.));
#17425=DIRECTION('ref_axis',(1.,0.,0.));
#21342=CARTESIAN_POINT('',(0.,0.,0.));
#21343=CARTESIAN_POINT('Origin',(10.7050737530542,0.8,17.1120538880616));
#21344=CARTESIAN_POINT('',(10.3550737530542,0.8,17.1120538880616));
#21345=CARTESIAN_POINT('Origin',(10.7050737530542,0.8,17.1120538880616));
#21346=CARTESIAN_POINT('',(10.5050737530542,0.8,17.1120538880616));
#21347=CARTESIAN_POINT('Origin',(10.7050737530542,0.8,17.1120538880616));
#21348=CARTESIAN_POINT('Origin',(10.7050737530542,0.8,17.1120538880616));
#21349=CARTESIAN_POINT('',(10.3550737530542,1.2,17.1120538880616));
#21350=CARTESIAN_POINT('Origin',(10.7050737530542,1.2,17.1120538880616));
#21351=CARTESIAN_POINT('',(10.3550737530542,0.8,17.1120538880616));
#21352=CARTESIAN_POINT('Origin',(10.7050737530542,1.2,17.1120538880616));
#21353=CARTESIAN_POINT('Origin',(10.7050737530542,0.1,17.1120538880616));
#21354=CARTESIAN_POINT('',(10.5050737530542,0.1,17.1120538880616));
#21355=CARTESIAN_POINT('',(10.5050737530542,0.1,17.1120538880616));
#21356=CARTESIAN_POINT('Origin',(10.7050737530542,0.1,17.1120538880616));
#21357=CARTESIAN_POINT('Origin',(10.7050737530542,0.1,17.1120538880616));
#23548=UNCERTAINTY_MEASURE_WITH_UNIT(LENGTH_MEASURE(0.001),#23729,
'DISTANCE_ACCURACY_VALUE',
'Maximum model space distance between geometric entities at asserted c
onnectivities');
#23611=UNCERTAINTY_MEASURE_WITH_UNIT(LENGTH_MEASURE(0.001),#23729,
'DISTANCE_ACCURACY_VALUE',
'Maximum model space distance between geometric entities at asserted c
onnectivities');
#23665=(
GEOMETRIC_REPRESENTATION_CONTEXT(3)
GLOBAL_UNCERTAINTY_ASSIGNED_CONTEXT((#23548))
GLOBAL_UNIT_ASSIGNED_CONTEXT((#23729,#23731,#23732))
REPRESENTATION_CONTEXT('','3D')
);
#23728=(
GEOMETRIC_REPRESENTATION_CONTEXT(3)
GLOBAL_UNCERTAINTY_ASSIGNED_CONTEXT((#23611))
GLOBAL_UNIT_ASSIGNED_CONTEXT((#23729,#23731,#23732))
REPRESENTATION_CONTEXT('','3D')
);
#23729=(
LENGTH_UNIT()
NAMED_UNIT(*)
SI_UNIT(.CENTI.,.METRE.)
);
#23731=(
NAMED_UNIT(*)
PLANE_ANGLE_UNIT()
SI_UNIT($,.RADIAN.)
);
#23732=(
NAMED_UNIT(*)
SI_UNIT($,.STERADIAN.)
SOLID_ANGLE_UNIT()
);
#23786=SHAPE_DEFINITION_REPRESENTATION(#23902,#24165);
#23902=PRODUCT_DEFINITION_SHAPE('',$,#24282);
#24165=SHAPE_REPRESENTATION('',(#14477),#23665);
#24228=PRODUCT_DEFINITION_CONTEXT('part definition',#24578,'design');
#24282=PRODUCT_DEFINITION('M4 short cap screw (15)',
'M4 short cap screw (15)',#24398,#24228);
#24398=PRODUCT_DEFINITION_FORMATION('',$,#24633);
#24578=APPLICATION_CONTEXT(
'Core Data for Automotive Mechanical Design Process');
#24579=PRODUCT_CONTEXT('part definition',#24578,'mechanical');
#24633=PRODUCT('M4 short cap screw (15)','M4 short cap screw (15)',
'M4 short cap screw (15)',(#24579));
#24766=COLOUR_RGB('Black',0.12,0.14,0.17);
#24767=FILL_AREA_STYLE_COLOUR('',#24766);
#24768=FILL_AREA_STYLE('',(#24767));
#24769=SURFACE_STYLE_FILL_AREA(#24768);
#24770=SURFACE_SIDE_STYLE('',(#24769));
#24771=SURFACE_STYLE_USAGE(.BOTH.,#24770);
#24772=PRESENTATION_STYLE_ASSIGNMENT((#24771));
ENDSEC;
END-ISO-10303-21;
